ISO-10303-21;
HEADER;
/* Generated by software containing ST-Developer
 * from STEP Tools, Inc. (www.steptools.com) 
 */

FILE_DESCRIPTION(
/* description */ (''),
/* implementation_level */ '2;1');

FILE_NAME(
/* name */ 'NUT.step',
/* time_stamp */ '2026-10-06T01:16:10-07:00',
/* author */ (''),
/* organization */ (''),
/* preprocessor_version */ 'ST-DEVELOPER v20.2',
/* originating_system */ 'Autodesk Translation Framework v15.15.0.0',
/* authorisation */ '');

FILE_SCHEMA (('AUTOMOTIVE_DESIGN { 1 0 10303 214 3 1 1 }'));
ENDSEC;

DATA;
#10=MECHANICAL_DESIGN_GEOMETRIC_PRESENTATION_REPRESENTATION('',(#320,#321),#17113);
#234=OPEN_SHELL('',(#5954,#5955));
#252=SHELL_BASED_SURFACE_MODEL('Body2',(#234));
#275=SHAPE_REPRESENTATION_RELATIONSHIP('SRR','None',#17200,#291);
#291=ADVANCED_BREP_SHAPE_REPRESENTATION('',(#341),#17107);
#320=STYLED_ITEM('',(#17298),#341);
#321=STYLED_ITEM('',(#17298),#252);
#341=MANIFOLD_SOLID_BREP('Body1',#6027);
#473=CYLINDRICAL_SURFACE('',#6821,1.75);
#474=CYLINDRICAL_SURFACE('',#6830,2.);
#616=FACE_BOUND('',#1770,.T.);
#617=FACE_BOUND('',#1773,.T.);
#618=FACE_BOUND('',#1782,.T.);
#938=CIRCLE('',#6820,1.75);
#939=CIRCLE('',#6822,1.75);
#940=CIRCLE('',#6831,2.);
#941=CIRCLE('',#6832,2.);
#942=CIRCLE('',#6834,1.75);
#1297=FACE_OUTER_BOUND('',#1769,.T.);
#1298=FACE_OUTER_BOUND('',#1771,.T.);
#1299=FACE_OUTER_BOUND('',#1772,.T.);
#1300=FACE_OUTER_BOUND('',#1774,.T.);
#1301=FACE_OUTER_BOUND('',#1775,.T.);
#1302=FACE_OUTER_BOUND('',#1776,.T.);
#1303=FACE_OUTER_BOUND('',#1777,.T.);
#1304=FACE_OUTER_BOUND('',#1778,.T.);
#1305=FACE_OUTER_BOUND('',#1779,.T.);
#1306=FACE_OUTER_BOUND('',#1780,.T.);
#1307=FACE_OUTER_BOUND('',#1781,.T.);
#1769=EDGE_LOOP('',(#5204,#5205,#5206,#5207,#5208,#5209));
#1770=EDGE_LOOP('',(#5210));
#1771=EDGE_LOOP('',(#5211,#5212,#5213,#5214));
#1772=EDGE_LOOP('',(#5215,#5216,#5217,#5218,#5219,#5220));
#1773=EDGE_LOOP('',(#5221));
#1774=EDGE_LOOP('',(#5222,#5223,#5224,#5225));
#1775=EDGE_LOOP('',(#5226,#5227,#5228,#5229));
#1776=EDGE_LOOP('',(#5230,#5231,#5232,#5233));
#1777=EDGE_LOOP('',(#5234,#5235,#5236,#5237));
#1778=EDGE_LOOP('',(#5238,#5239,#5240,#5241));
#1779=EDGE_LOOP('',(#5242,#5243,#5244,#5245));
#1780=EDGE_LOOP('',(#5246,#5247,#5248,#5249));
#1781=EDGE_LOOP('',(#5250));
#1782=EDGE_LOOP('',(#5251));
#2140=LINE('',#16711,#2501);
#2141=LINE('',#16713,#2502);
#2142=LINE('',#16715,#2503);
#2143=LINE('',#16717,#2504);
#2144=LINE('',#16719,#2505);
#2145=LINE('',#16720,#2506);
#2146=LINE('',#16725,#2507);
#2147=LINE('',#16730,#2508);
#2148=LINE('',#16732,#2509);
#2149=LINE('',#16734,#2510);
#2150=LINE('',#16736,#2511);
#2151=LINE('',#16738,#2512);
#2152=LINE('',#16739,#2513);
#2153=LINE('',#16741,#2514);
#2154=LINE('',#16742,#2515);
#2155=LINE('',#16744,#2516);
#2156=LINE('',#16746,#2517);
#2157=LINE('',#16748,#2518);
#2158=LINE('',#16750,#2519);
#2159=LINE('',#16756,#2520);
#2501=VECTOR('',#8480,4.);
#2502=VECTOR('',#8481,3.99999999999987);
#2503=VECTOR('',#8482,3.99999999999987);
#2504=VECTOR('',#8483,4.);
#2505=VECTOR('',#8484,3.99999999999987);
#2506=VECTOR('',#8485,3.99999999999987);
#2507=VECTOR('',#8490,1.75);
#2508=VECTOR('',#8495,4.);
#2509=VECTOR('',#8496,3.99999999999987);
#2510=VECTOR('',#8497,3.99999999999987);
#2511=VECTOR('',#8498,4.);
#2512=VECTOR('',#8499,3.99999999999987);
#2513=VECTOR('',#8500,3.99999999999987);
#2514=VECTOR('',#8503,4.);
#2515=VECTOR('',#8504,4.);
#2516=VECTOR('',#8507,4.);
#2517=VECTOR('',#8510,4.);
#2518=VECTOR('',#8513,4.);
#2519=VECTOR('',#8516,4.);
#2520=VECTOR('',#8523,2.);
#3000=VERTEX_POINT('',#16709);
#3001=VERTEX_POINT('',#16710);
#3002=VERTEX_POINT('',#16712);
#3003=VERTEX_POINT('',#16714);
#3004=VERTEX_POINT('',#16716);
#3005=VERTEX_POINT('',#16718);
#3006=VERTEX_POINT('',#16721);
#3007=VERTEX_POINT('',#16724);
#3008=VERTEX_POINT('',#16728);
#3009=VERTEX_POINT('',#16729);
#3010=VERTEX_POINT('',#16731);
#3011=VERTEX_POINT('',#16733);
#3012=VERTEX_POINT('',#16735);
#3013=VERTEX_POINT('',#16737);
#3014=VERTEX_POINT('',#16753);
#3015=VERTEX_POINT('',#16755);
#3016=VERTEX_POINT('',#16759);
#3761=EDGE_CURVE('',#3000,#3001,#2140,.T.);
#3762=EDGE_CURVE('',#3002,#3000,#2141,.T.);
#3763=EDGE_CURVE('',#3003,#3002,#2142,.T.);
#3764=EDGE_CURVE('',#3004,#3003,#2143,.T.);
#3765=EDGE_CURVE('',#3005,#3004,#2144,.T.);
#3766=EDGE_CURVE('',#3001,#3005,#2145,.T.);
#3767=EDGE_CURVE('',#3006,#3006,#938,.T.);
#3768=EDGE_CURVE('',#3006,#3007,#2146,.T.);
#3769=EDGE_CURVE('',#3007,#3007,#939,.T.);
#3770=EDGE_CURVE('',#3008,#3009,#2147,.T.);
#3771=EDGE_CURVE('',#3009,#3010,#2148,.T.);
#3772=EDGE_CURVE('',#3010,#3011,#2149,.T.);
#3773=EDGE_CURVE('',#3011,#3012,#2150,.T.);
#3774=EDGE_CURVE('',#3012,#3013,#2151,.T.);
#3775=EDGE_CURVE('',#3013,#3008,#2152,.T.);
#3776=EDGE_CURVE('',#3001,#3009,#2153,.T.);
#3777=EDGE_CURVE('',#3000,#3008,#2154,.T.);
#3778=EDGE_CURVE('',#3002,#3013,#2155,.T.);
#3779=EDGE_CURVE('',#3003,#3012,#2156,.T.);
#3780=EDGE_CURVE('',#3004,#3011,#2157,.T.);
#3781=EDGE_CURVE('',#3005,#3010,#2158,.T.);
#3782=EDGE_CURVE('',#3014,#3014,#940,.T.);
#3783=EDGE_CURVE('',#3014,#3015,#2159,.T.);
#3784=EDGE_CURVE('',#3015,#3015,#941,.T.);
#3785=EDGE_CURVE('',#3016,#3016,#942,.T.);
#5204=ORIENTED_EDGE('',*,*,#3761,.F.);
#5205=ORIENTED_EDGE('',*,*,#3762,.F.);
#5206=ORIENTED_EDGE('',*,*,#3763,.F.);
#5207=ORIENTED_EDGE('',*,*,#3764,.F.);
#5208=ORIENTED_EDGE('',*,*,#3765,.F.);
#5209=ORIENTED_EDGE('',*,*,#3766,.F.);
#5210=ORIENTED_EDGE('',*,*,#3767,.F.);
#5211=ORIENTED_EDGE('',*,*,#3767,.T.);
#5212=ORIENTED_EDGE('',*,*,#3768,.T.);
#5213=ORIENTED_EDGE('',*,*,#3769,.F.);
#5214=ORIENTED_EDGE('',*,*,#3768,.F.);
#5215=ORIENTED_EDGE('',*,*,#3770,.T.);
#5216=ORIENTED_EDGE('',*,*,#3771,.T.);
#5217=ORIENTED_EDGE('',*,*,#3772,.T.);
#5218=ORIENTED_EDGE('',*,*,#3773,.T.);
#5219=ORIENTED_EDGE('',*,*,#3774,.T.);
#5220=ORIENTED_EDGE('',*,*,#3775,.T.);
#5221=ORIENTED_EDGE('',*,*,#3769,.T.);
#5222=ORIENTED_EDGE('',*,*,#3761,.T.);
#5223=ORIENTED_EDGE('',*,*,#3776,.T.);
#5224=ORIENTED_EDGE('',*,*,#3770,.F.);
#5225=ORIENTED_EDGE('',*,*,#3777,.F.);
#5226=ORIENTED_EDGE('',*,*,#3762,.T.);
#5227=ORIENTED_EDGE('',*,*,#3777,.T.);
#5228=ORIENTED_EDGE('',*,*,#3775,.F.);
#5229=ORIENTED_EDGE('',*,*,#3778,.F.);
#5230=ORIENTED_EDGE('',*,*,#3763,.T.);
#5231=ORIENTED_EDGE('',*,*,#3778,.T.);
#5232=ORIENTED_EDGE('',*,*,#3774,.F.);
#5233=ORIENTED_EDGE('',*,*,#3779,.F.);
#5234=ORIENTED_EDGE('',*,*,#3764,.T.);
#5235=ORIENTED_EDGE('',*,*,#3779,.T.);
#5236=ORIENTED_EDGE('',*,*,#3773,.F.);
#5237=ORIENTED_EDGE('',*,*,#3780,.F.);
#5238=ORIENTED_EDGE('',*,*,#3765,.T.);
#5239=ORIENTED_EDGE('',*,*,#3780,.T.);
#5240=ORIENTED_EDGE('',*,*,#3772,.F.);
#5241=ORIENTED_EDGE('',*,*,#3781,.F.);
#5242=ORIENTED_EDGE('',*,*,#3766,.T.);
#5243=ORIENTED_EDGE('',*,*,#3781,.T.);
#5244=ORIENTED_EDGE('',*,*,#3771,.F.);
#5245=ORIENTED_EDGE('',*,*,#3776,.F.);
#5246=ORIENTED_EDGE('',*,*,#3782,.F.);
#5247=ORIENTED_EDGE('',*,*,#3783,.T.);
#5248=ORIENTED_EDGE('',*,*,#3784,.T.);
#5249=ORIENTED_EDGE('',*,*,#3783,.F.);
#5250=ORIENTED_EDGE('',*,*,#3784,.F.);
#5251=ORIENTED_EDGE('',*,*,#3785,.F.);
#5618=PLANE('',#6819);
#5619=PLANE('',#6823);
#5620=PLANE('',#6824);
#5621=PLANE('',#6825);
#5622=PLANE('',#6826);
#5623=PLANE('',#6827);
#5624=PLANE('',#6828);
#5625=PLANE('',#6829);
#5626=PLANE('',#6833);
#5945=ADVANCED_FACE('',(#1297,#616),#5618,.F.);
#5946=ADVANCED_FACE('',(#1298),#473,.F.);
#5947=ADVANCED_FACE('',(#1299,#617),#5619,.T.);
#5948=ADVANCED_FACE('',(#1300),#5620,.T.);
#5949=ADVANCED_FACE('',(#1301),#5621,.T.);
#5950=ADVANCED_FACE('',(#1302),#5622,.T.);
#5951=ADVANCED_FACE('',(#1303),#5623,.T.);
#5952=ADVANCED_FACE('',(#1304),#5624,.T.);
#5953=ADVANCED_FACE('',(#1305),#5625,.T.);
#5954=ADVANCED_FACE('',(#1306),#474,.T.);
#5955=ADVANCED_FACE('',(#1307,#618),#5626,.F.);
#6027=CLOSED_SHELL('',(#5945,#5946,#5947,#5948,#5949,#5950,#5951,#5952,
#5953));
#6818=AXIS2_PLACEMENT_3D('',#16707,#8476,#8477);
#6819=AXIS2_PLACEMENT_3D('',#16708,#8478,#8479);
#6820=AXIS2_PLACEMENT_3D('',#16722,#8486,#8487);
#6821=AXIS2_PLACEMENT_3D('',#16723,#8488,#8489);
#6822=AXIS2_PLACEMENT_3D('',#16726,#8491,#8492);
#6823=AXIS2_PLACEMENT_3D('',#16727,#8493,#8494);
#6824=AXIS2_PLACEMENT_3D('',#16740,#8501,#8502);
#6825=AXIS2_PLACEMENT_3D('',#16743,#8505,#8506);
#6826=AXIS2_PLACEMENT_3D('',#16745,#8508,#8509);
#6827=AXIS2_PLACEMENT_3D('',#16747,#8511,#8512);
#6828=AXIS2_PLACEMENT_3D('',#16749,#8514,#8515);
#6829=AXIS2_PLACEMENT_3D('',#16751,#8517,#8518);
#6830=AXIS2_PLACEMENT_3D('',#16752,#8519,#8520);
#6831=AXIS2_PLACEMENT_3D('',#16754,#8521,#8522);
#6832=AXIS2_PLACEMENT_3D('',#16757,#8524,#8525);
#6833=AXIS2_PLACEMENT_3D('',#16758,#8526,#8527);
#6834=AXIS2_PLACEMENT_3D('',#16760,#8528,#8529);
#8476=DIRECTION('axis',(0.,0.,1.));
#8477=DIRECTION('refdir',(1.,0.,0.));
#8478=DIRECTION('center_axis',(0.,0.,1.));
#8479=DIRECTION('ref_axis',(1.,0.,0.));
#8480=DIRECTION('',(1.,0.,0.));
#8481=DIRECTION('',(0.500000000000017,-0.866025403784429,0.));
#8482=DIRECTION('',(-0.500000000000017,-0.866025403784429,0.));
#8483=DIRECTION('',(-1.,0.,0.));
#8484=DIRECTION('',(-0.500000000000017,0.866025403784429,0.));
#8485=DIRECTION('',(0.500000000000017,0.866025403784429,0.));
#8486=DIRECTION('center_axis',(0.,0.,-1.));
#8487=DIRECTION('ref_axis',(1.,0.,0.));
#8488=DIRECTION('center_axis',(0.,0.,1.));
#8489=DIRECTION('ref_axis',(1.,0.,0.));
#8490=DIRECTION('',(0.,0.,1.));
#8491=DIRECTION('center_axis',(0.,0.,-1.));
#8492=DIRECTION('ref_axis',(1.,0.,0.));
#8493=DIRECTION('center_axis',(0.,0.,1.));
#8494=DIRECTION('ref_axis',(1.,0.,0.));
#8495=DIRECTION('',(1.,0.,0.));
#8496=DIRECTION('',(0.500000000000017,0.866025403784429,0.));
#8497=DIRECTION('',(-0.500000000000017,0.866025403784429,0.));
#8498=DIRECTION('',(-1.,0.,0.));
#8499=DIRECTION('',(-0.500000000000017,-0.866025403784429,0.));
#8500=DIRECTION('',(0.500000000000017,-0.866025403784429,0.));
#8501=DIRECTION('center_axis',(0.,-1.,0.));
#8502=DIRECTION('ref_axis',(1.,0.,0.));
#8503=DIRECTION('',(0.,0.,1.));
#8504=DIRECTION('',(0.,0.,1.));
#8505=DIRECTION('center_axis',(-0.866025403784429,-0.500000000000017,0.));
#8506=DIRECTION('ref_axis',(0.500000000000017,-0.866025403784429,0.));
#8507=DIRECTION('',(0.,0.,1.));
#8508=DIRECTION('center_axis',(-0.866025403784429,0.500000000000017,0.));
#8509=DIRECTION('ref_axis',(-0.500000000000017,-0.866025403784429,0.));
#8510=DIRECTION('',(0.,0.,1.));
#8511=DIRECTION('center_axis',(0.,1.,0.));
#8512=DIRECTION('ref_axis',(-1.,0.,0.));
#8513=DIRECTION('',(0.,0.,1.));
#8514=DIRECTION('center_axis',(0.866025403784429,0.500000000000017,0.));
#8515=DIRECTION('ref_axis',(-0.500000000000017,0.866025403784429,0.));
#8516=DIRECTION('',(0.,0.,1.));
#8517=DIRECTION('center_axis',(0.866025403784429,-0.500000000000017,0.));
#8518=DIRECTION('ref_axis',(0.500000000000017,0.866025403784429,0.));
#8519=DIRECTION('center_axis',(0.,0.,1.));
#8520=DIRECTION('ref_axis',(1.,0.,0.));
#8521=DIRECTION('center_axis',(0.,0.,1.));
#8522=DIRECTION('ref_axis',(-1.,0.,0.));
#8523=DIRECTION('',(0.,0.,-1.));
#8524=DIRECTION('center_axis',(0.,0.,1.));
#8525=DIRECTION('ref_axis',(-1.,0.,0.));
#8526=DIRECTION('center_axis',(0.,0.,1.));
#8527=DIRECTION('ref_axis',(1.,0.,0.));
#8528=DIRECTION('center_axis',(0.,0.,-1.));
#8529=DIRECTION('ref_axis',(-1.,0.,0.));
#16707=CARTESIAN_POINT('',(0.,0.,0.));
#16708=CARTESIAN_POINT('Origin',(0.,0.,0.));
#16709=CARTESIAN_POINT('',(-2.,-3.464101615138,0.));
#16710=CARTESIAN_POINT('',(2.,-3.464101615138,0.));
#16711=CARTESIAN_POINT('',(-2.,-3.464101615138,0.));
#16712=CARTESIAN_POINT('',(-4.,0.,0.));
#16713=CARTESIAN_POINT('',(-4.,0.,0.));
#16714=CARTESIAN_POINT('',(-2.,3.464101615138,0.));
#16715=CARTESIAN_POINT('',(-2.,3.464101615138,0.));
#16716=CARTESIAN_POINT('',(2.,3.464101615138,0.));
#16717=CARTESIAN_POINT('',(2.,3.464101615138,0.));
#16718=CARTESIAN_POINT('',(4.,0.,0.));
#16719=CARTESIAN_POINT('',(4.,0.,0.));
#16720=CARTESIAN_POINT('',(2.,-3.464101615138,0.));
#16721=CARTESIAN_POINT('',(-1.75,-2.14313189850787E-16,0.));
#16722=CARTESIAN_POINT('Origin',(0.,0.,0.));
#16723=CARTESIAN_POINT('Origin',(0.,0.,0.));
#16724=CARTESIAN_POINT('',(-1.75,-2.14313189850787E-16,4.));
#16725=CARTESIAN_POINT('',(-1.75,-2.14313189850787E-16,0.));
#16726=CARTESIAN_POINT('Origin',(0.,0.,4.));
#16727=CARTESIAN_POINT('Origin',(0.,0.,4.));
#16728=CARTESIAN_POINT('',(-2.,-3.464101615138,4.));
#16729=CARTESIAN_POINT('',(2.,-3.464101615138,4.));
#16730=CARTESIAN_POINT('',(-2.,-3.464101615138,4.));
#16731=CARTESIAN_POINT('',(4.,0.,4.));
#16732=CARTESIAN_POINT('',(2.,-3.464101615138,4.));
#16733=CARTESIAN_POINT('',(2.,3.464101615138,4.));
#16734=CARTESIAN_POINT('',(4.,0.,4.));
#16735=CARTESIAN_POINT('',(-2.,3.464101615138,4.));
#16736=CARTESIAN_POINT('',(2.,3.464101615138,4.));
#16737=CARTESIAN_POINT('',(-4.,0.,4.));
#16738=CARTESIAN_POINT('',(-2.,3.464101615138,4.));
#16739=CARTESIAN_POINT('',(-4.,0.,4.));
#16740=CARTESIAN_POINT('Origin',(-2.,-3.464101615138,0.));
#16741=CARTESIAN_POINT('',(2.,-3.464101615138,0.));
#16742=CARTESIAN_POINT('',(-2.,-3.464101615138,0.));
#16743=CARTESIAN_POINT('Origin',(-4.,0.,0.));
#16744=CARTESIAN_POINT('',(-4.,0.,0.));
#16745=CARTESIAN_POINT('Origin',(-2.,3.464101615138,0.));
#16746=CARTESIAN_POINT('',(-2.,3.464101615138,0.));
#16747=CARTESIAN_POINT('Origin',(2.,3.464101615138,0.));
#16748=CARTESIAN_POINT('',(2.,3.464101615138,0.));
#16749=CARTESIAN_POINT('Origin',(4.,0.,0.));
#16750=CARTESIAN_POINT('',(4.,0.,0.));
#16751=CARTESIAN_POINT('Origin',(2.,-3.464101615138,0.));
#16752=CARTESIAN_POINT('Origin',(0.,0.,4.));
#16753=CARTESIAN_POINT('',(-2.,-2.44929359829471E-16,4.));
#16754=CARTESIAN_POINT('Origin',(0.,0.,4.));
#16755=CARTESIAN_POINT('',(-2.,-2.44929359829471E-16,0.));
#16756=CARTESIAN_POINT('',(-2.,-2.44929359829471E-16,4.));
#16757=CARTESIAN_POINT('Origin',(0.,0.,0.));
#16758=CARTESIAN_POINT('Origin',(0.,0.,0.));
#16759=CARTESIAN_POINT('',(1.75,0.,0.));
#16760=CARTESIAN_POINT('Origin',(0.,0.,0.));
#17084=UNCERTAINTY_MEASURE_WITH_UNIT(LENGTH_MEASURE(0.01),#17114,
'DISTANCE_ACCURACY_VALUE',
'Maximum model space distance between geometric entities at asserted c
onnectivities');
#17090=UNCERTAINTY_MEASURE_WITH_UNIT(LENGTH_MEASURE(0.01),#17114,
'DISTANCE_ACCURACY_VALUE',
'Maximum model space distance between geometric entities at asserted c
onnectivities');
#17107=(
GEOMETRIC_REPRESENTATION_CONTEXT(3)
GLOBAL_UNCERTAINTY_ASSIGNED_CONTEXT((#17084))
GLOBAL_UNIT_ASSIGNED_CONTEXT((#17114,#17116,#17117))
REPRESENTATION_CONTEXT('','3D')
);
#17113=(
GEOMETRIC_REPRESENTATION_CONTEXT(3)
GLOBAL_UNCERTAINTY_ASSIGNED_CONTEXT((#17090))
GLOBAL_UNIT_ASSIGNED_CONTEXT((#17114,#17116,#17117))
REPRESENTATION_CONTEXT('','3D')
);
#17114=(
LENGTH_UNIT()
NAMED_UNIT(*)
SI_UNIT(.MILLI.,.METRE.)
);
#17116=(
NAMED_UNIT(*)
PLANE_ANGLE_UNIT()
SI_UNIT($,.RADIAN.)
);
#17117=(
NAMED_UNIT(*)
SI_UNIT($,.STERADIAN.)
SOLID_ANGLE_UNIT()
);
#17134=SHAPE_DEFINITION_REPRESENTATION(#17165,#17200);
#17165=PRODUCT_DEFINITION_SHAPE('',$,#17223);
#17200=SHAPE_REPRESENTATION('',(#6818,#252),#17107);
#17206=PRODUCT_DEFINITION_CONTEXT('part definition',#17274,'design');
#17223=PRODUCT_DEFINITION('Nut','NUT',#17245,#17206);
#17245=PRODUCT_DEFINITION_FORMATION('',$,#17292);
#17274=APPLICATION_CONTEXT(
'Core Data for Automotive Mechanical Design Process');
#17275=PRODUCT_CONTEXT('part definition',#17274,'mechanical');
#17292=PRODUCT('Nut','NUT',$,(#17275));
#17298=PRESENTATION_STYLE_ASSIGNMENT((#17299));
#17299=SURFACE_STYLE_USAGE(.BOTH.,#17300);
#17300=SURFACE_SIDE_STYLE('',(#17301));
#17301=SURFACE_STYLE_FILL_AREA(#17302);
#17302=FILL_AREA_STYLE('Steel - Satin',(#17303));
#17303=FILL_AREA_STYLE_COLOUR('Steel - Satin',#17304);
#17304=COLOUR_RGB('Steel - Satin', 0.09019608, 0.27058824, 0.51372549);
ENDSEC;
END-ISO-10303-21;
